ISO-10303-21;
HEADER;
FILE_DESCRIPTION (('STEP AP214'),
    '1' );
FILE_NAME ('circlip for shafts normal_din_Circlip DIN 471 - 50 x 2.step',
    '2026-10-24T07:08:27',
    ( '' ),
    ( '' ),
    'SwSTEP 2.0',
    'SolidWorks 2026',
    '' );
FILE_SCHEMA (( 'AUTOMOTIVE_DESIGN' ));
ENDSEC;

DATA;
#52=CARTESIAN_POINT ( 'NONE',  ( 9.345251662538453630, -28.92794965710190525, -2.000000000000000000 ) ) ;
#96=DIRECTION ( 'NONE',  ( 0.000000000000000000, 0.000000000000000000, 1.000000000000000000 ) ) ;
#148=( GEOMETRIC_REPRESENTATION_CONTEXT ( 3 ) GLOBAL_UNCERTAINTY_ASSIGNED_CONTEXT ( ( #11684 ) ) GLOBAL_UNIT_ASSIGNED_CONTEXT ( ( #18254, #15584, #13862 ) ) REPRESENTATION_CONTEXT ( 'NONE', 'WORKASPACE' ) );
#199=MECHANICAL_DESIGN_GEOMETRIC_PRESENTATION_REPRESENTATION('',(#3240),#15710);
#252=AXIS2_PLACEMENT_3D ( 'NONE', #13073, #8403, #2977 ) ;
#265=CIRCLE ( 'NONE', #10902, 23.50000000000000355 ) ;
#280=VERTEX_POINT ( 'NONE', #17994 ) ;
#284=FACE_OUTER_BOUND ( 'NONE', #13491, .T. ) ;
#296=AXIS2_PLACEMENT_3D ( 'NONE', #5203, #15025, #16454 ) ;
#298=VERTEX_POINT ( 'NONE', #12276 ) ;
#308=DIRECTION ( 'NONE',  ( 1.000000000000000000, 0.000000000000000000, 0.000000000000000000 ) ) ;
#326=LINE ( 'NONE', #14699, #2052 ) ;
#329=CARTESIAN_POINT ( 'NONE',  ( 0.000000000000000000, 0.000000000000000000, -2.000000000000000000 ) ) ;
#355=CARTESIAN_POINT ( 'NONE',  ( -27.29487558977753991, 1.305124410222464393, -2.000000000000000000 ) ) ;
#367=DIRECTION ( 'NONE',  ( -0.9998647328874151752, -0.01644736842105263067, 0.000000000000000000 ) ) ;
#406=EDGE_LOOP ( 'NONE', ( #5497, #14541, #4371, #16219 ) ) ;
#416=CARTESIAN_POINT ( 'NONE',  ( 4.249769933734876659, -30.10148593525447680, -2.000000000000000000 ) ) ;
#457=ORIENTED_EDGE ( 'NONE', *, *, #6226, .F. ) ;
#461=DIRECTION ( 'NONE',  ( 0.000000000000000000, 0.000000000000000000, 1.000000000000000000 ) ) ;
#492=ORIENTED_EDGE ( 'NONE', *, *, #2597, .T. ) ;
#508=LINE ( 'NONE', #698, #14239 ) ;
#551=CARTESIAN_POINT ( 'NONE',  ( 0.3865131578947368918, -23.49682122285426189, -2.000000000000000000 ) ) ;
#572=CIRCLE ( 'NONE', #17307, 1.250000000000001110 ) ;
#596=VERTEX_POINT ( 'NONE', #6138 ) ;
#604=DIRECTION ( 'NONE',  ( 0.000000000000000000, 0.000000000000000000, 1.000000000000000000 ) ) ;
#644=EDGE_CURVE ( 'NONE', #280, #4113, #4330, .T. ) ;
#649=AXIS2_PLACEMENT_3D ( 'NONE', #4437, #7479, #13300 ) ;
#656=CARTESIAN_POINT ( 'NONE',  ( -0.3865131578947368918, -23.49682122285426189, 0.000000000000000000 ) ) ;
#676=AXIS2_PLACEMENT_3D ( 'NONE', #14556, #1514, #13044 ) ;
#677=DIRECTION ( 'NONE',  ( 1.000000000000000000, 0.000000000000000000, 0.000000000000000000 ) ) ;
#688=ORIENTED_EDGE ( 'NONE', *, *, #12289, .T. ) ;
#698=CARTESIAN_POINT ( 'NONE',  ( -4.249769933734879324, -30.10148593525447680, -2.000000000000000000 ) ) ;
#736=( NAMED_UNIT ( * ) SI_UNIT ( $, .STERADIAN. ) SOLID_ANGLE_UNIT ( ) );
#741=FACE_OUTER_BOUND ( 'NONE', #7620, .T. ) ;
#782=ORIENTED_EDGE ( 'NONE', *, *, #1620, .F. ) ;
#843=CIRCLE ( 'NONE', #12385, 1.249999999999999778 ) ;
#867=CIRCLE ( 'NONE', #8153, 4.349594641156947716 ) ;
#906=VERTEX_POINT ( 'NONE', #8420 ) ;
#936=ORIENTED_EDGE ( 'NONE', *, *, #11799, .F. ) ;
#963=CARTESIAN_POINT ( 'NONE',  ( 4.144923636027600722, -29.35885059145708098, 0.000000000000000000 ) ) ;
#1018=VERTEX_POINT ( 'NONE', #15155 ) ;
#1033=DIRECTION ( 'NONE',  ( 0.000000000000000000, 0.000000000000000000, 1.000000000000000000 ) ) ;
#1039=FACE_OUTER_BOUND ( 'NONE', #2644, .T. ) ;
#1041=ORIENTED_EDGE ( 'NONE', *, *, #1490, .T. ) ;
#1156=CARTESIAN_POINT ( 'NONE',  ( 0.000000000000000000, 0.000000000000000000, -2.000000000000000000 ) ) ;
#1189=ORIENTED_EDGE ( 'NONE', *, *, #10587, .T. ) ;
#1201=DIRECTION ( 'NONE',  ( 1.000000000000000000, 0.000000000000000000, 0.000000000000000000 ) ) ;
#1213=ADVANCED_FACE ( 'NONE', ( #14194 ), #4377, .T. ) ;
#1229=ORIENTED_EDGE ( 'NONE', *, *, #1432, .F. ) ;
#1342=DIRECTION ( 'NONE',  ( 0.000000000000000000, 0.000000000000000000, 1.000000000000000000 ) ) ;
#1413=VECTOR ( 'NONE', #3052, 1000.000000000000000 ) ;
#1432=EDGE_CURVE ( 'NONE', #9337, #5360, #326, .T. ) ;
#1435=VERTEX_POINT ( 'NONE', #14273 ) ;
#1487=CIRCLE ( 'NONE', #6349, 23.50000000000000355 ) ;
#1490=EDGE_CURVE ( 'NONE', #6043, #18269, #12019, .T. ) ;
#1514=DIRECTION ( 'NONE',  ( 0.000000000000000000, 0.000000000000000000, 1.000000000000000000 ) ) ;
#1565=DIRECTION ( 'NONE',  ( 0.000000000000000000, 0.000000000000000000, 1.000000000000000000 ) ) ;
#1566=LINE ( 'NONE', #416, #3002 ) ;
#1581=FACE_OUTER_BOUND ( 'NONE', #16566, .T. ) ;
#1620=EDGE_CURVE ( 'NONE', #3988, #12362, #508, .T. ) ;
#1720=CARTESIAN_POINT ( 'NONE',  ( 0.000000000000000000, 0.000000000000000000, -2.000000000000000000 ) ) ;
#1742=CARTESIAN_POINT ( 'NONE',  ( -5.032868406504333869, -28.36021363089093938, 0.000000000000000000 ) ) ;
#1745=PLANE ( 'NONE',  #16514 ) ;
#1802=PLANE ( 'NONE',  #11541 ) ;
#1820=CYLINDRICAL_SURFACE ( 'NONE', #8160, 30.39999999999999858 ) ;
#1823=CARTESIAN_POINT ( 'NONE',  ( -4.888507282057958037, -29.45674523562211888, -2.000000000000000000 ) ) ;
#1851=CARTESIAN_POINT ( 'NONE',  ( 27.29487558977753991, 1.305124410222461284, -2.000000000000000000 ) ) ;
#1854=DIRECTION ( 'NONE',  ( 0.000000000000000000, 0.000000000000000000, 1.000000000000000000 ) ) ;
#1856=EDGE_CURVE ( 'NONE', #4661, #17469, #8681, .T. ) ;
#1881=CARTESIAN_POINT ( 'NONE',  ( -5.032868406504333869, -28.36021363089093938, 0.000000000000000000 ) ) ;
#1888=DIRECTION ( 'NONE',  ( 1.000000000000000000, 0.000000000000000000, 0.000000000000000000 ) ) ;
#1894=DIRECTION ( 'NONE',  ( -0.000000000000000000, -0.000000000000000000, -1.000000000000000000 ) ) ;
#1900=ORIENTED_EDGE ( 'NONE', *, *, #4923, .T. ) ;
#1924=ORIENTED_EDGE ( 'NONE', *, *, #7619, .F. ) ;
#1950=EDGE_LOOP ( 'NONE', ( #1924, #2038, #16540, #17201 ) ) ;
#2010=AXIS2_PLACEMENT_3D ( 'NONE', #5080, #9754, #9655 ) ;
#2038=ORIENTED_EDGE ( 'NONE', *, *, #11988, .F. ) ;
#2044=ADVANCED_FACE ( 'NONE', ( #15055 ), #1820, .T. ) ;
#2052=VECTOR ( 'NONE', #11216, 1000.000000000000000 ) ;
#2057=LINE ( 'NONE', #3485, #10083 ) ;
#2115=EDGE_CURVE ( 'NONE', #2471, #280, #4810, .T. ) ;
#2193=CARTESIAN_POINT ( 'NONE',  ( 9.345251662538453630, -28.92794965710190525, 0.000000000000000000 ) ) ;
#2205=VECTOR ( 'NONE', #8271, 1000.000000000000000 ) ;
#2266=ORIENTED_EDGE ( 'NONE', *, *, #2115, .F. ) ;
#2326=CARTESIAN_POINT ( 'NONE',  ( -0.3865131578947368918, -23.49682122285426189, -2.000000000000000000 ) ) ;
#2386=SHAPE_REPRESENTATION ( 'circlip for shafts normal_din_Circlip DIN 471 - 50 x 2', ( #8017 ), #3170 ) ;
#2388=FACE_OUTER_BOUND ( 'NONE', #13778, .T. ) ;
#2402=AXIS2_PLACEMENT_3D ( 'NONE', #8200, #11134, #9718 ) ;
#2433=CYLINDRICAL_SURFACE ( 'NONE', #18608, 0.7499999999999997780 ) ;
#2442=ORIENTED_EDGE ( 'NONE', *, *, #12289, .F. ) ;
#2450=ORIENTED_EDGE ( 'NONE', *, *, #17509, .F. ) ;
#2458=DIRECTION ( 'NONE',  ( -0.000000000000000000, -0.000000000000000000, -1.000000000000000000 ) ) ;
#2465=ADVANCED_FACE ( 'NONE', ( #284 ), #10653, .T. ) ;
#2467=CARTESIAN_POINT ( 'NONE',  ( 5.032868406504333869, -28.36021363089093938, -2.000000000000000000 ) ) ;
#2471=VERTEX_POINT ( 'NONE', #8932 ) ;
#2480=ORIENTED_EDGE ( 'NONE', *, *, #10652, .T. ) ;
#2485=CIRCLE ( 'NONE', #15568, 30.39999999999999858 ) ;
#2505=DIRECTION ( 'NONE',  ( 1.000000000000000000, 0.000000000000000000, 0.000000000000000000 ) ) ;
#2516=ADVANCED_FACE ( 'NONE', ( #15138 ), #1802, .T. ) ;
#2597=EDGE_CURVE ( 'NONE', #9337, #10165, #1487, .T. ) ;
#2636=ORIENTED_EDGE ( 'NONE', *, *, #15650, .T. ) ;
#2642=CARTESIAN_POINT ( 'NONE',  ( 2.250000000000000000, -27.60846790388774608, 0.000000000000000000 ) ) ;
#2644=EDGE_LOOP ( 'NONE', ( #18035, #9393, #17813, #7720 ) ) ;
#2659=CIRCLE ( 'NONE', #15738, 27.29487558977753991 ) ;
#2697=CARTESIAN_POINT ( 'NONE',  ( -0.3865131578947368918, -23.49682122285426189, -2.000000000000000000 ) ) ;
#2700=ORIENTED_EDGE ( 'NONE', *, *, #6226, .T. ) ;
#2702=AXIS2_PLACEMENT_3D ( 'NONE', #329, #3468, #11936 ) ;
#2717=DIRECTION ( 'NONE',  ( 0.000000000000000000, 0.000000000000000000, 1.000000000000000000 ) ) ;
#2728=FILL_AREA_STYLE_COLOUR ( '', #8034 ) ;
#2774=FACE_OUTER_BOUND ( 'NONE', #18273, .T. ) ;
#2847=CYLINDRICAL_SURFACE ( 'NONE', #676, 27.29487558977753991 ) ;
#2870=ORIENTED_EDGE ( 'NONE', *, *, #17509, .T. ) ;
#2899=ORIENTED_EDGE ( 'NONE', *, *, #15271, .F. ) ;
#2919=LINE ( 'NONE', #8726, #13319 ) ;
#2948=CARTESIAN_POINT ( 'NONE',  ( -2.250000000000000000, -27.60846790388774608, 0.000000000000000000 ) ) ;
#2977=DIRECTION ( 'NONE',  ( 1.000000000000000000, 0.000000000000000000, 0.000000000000000000 ) ) ;
#3002=VECTOR ( 'NONE', #17940, 1000.000000000000000 ) ;
#3052=DIRECTION ( 'NONE',  ( 0.000000000000000000, 0.000000000000000000, 1.000000000000000000 ) ) ;
#3082=PRODUCT_CONTEXT ( 'NONE', #12791, 'mechanical' ) ;
#3095=CIRCLE ( 'NONE', #15256, 23.50000000000000355 ) ;
#3165=ORIENTED_EDGE ( 'NONE', *, *, #10662, .T. ) ;
#3170=( GEOMETRIC_REPRESENTATION_CONTEXT ( 3 ) GLOBAL_UNCERTAINTY_ASSIGNED_CONTEXT ( ( #17765 ) ) GLOBAL_UNIT_ASSIGNED_CONTEXT ( ( #7673, #10718, #736 ) ) REPRESENTATION_CONTEXT ( 'NONE', 'WORKASPACE' ) );
#3178=FACE_BOUND ( 'NONE', #15130, .T. ) ;
#3231=DIRECTION ( 'NONE',  ( -0.000000000000000000, -0.000000000000000000, -1.000000000000000000 ) ) ;
#3240=STYLED_ITEM('',(#18876),#3564);
#3373=ORIENTED_EDGE ( 'NONE', *, *, #5819, .F. ) ;
#3421=DIRECTION ( 'NONE',  ( 0.000000000000000000, 0.000000000000000000, 1.000000000000000000 ) ) ;
#3453=AXIS2_PLACEMENT_3D ( 'NONE', #13263, #10142, #15949 ) ;
#3468=DIRECTION ( 'NONE',  ( 0.000000000000000000, 0.000000000000000000, 1.000000000000000000 ) ) ;
#3485=CARTESIAN_POINT ( 'NONE',  ( 23.50000000000000355, 0.000000000000000000, -2.000000000000000000 ) ) ;
#3508=LINE ( 'NONE', #17893, #3874 ) ;
#3534=CARTESIAN_POINT ( 'NONE',  ( 8.060728450267873768, -24.77235419320996357, -2.000000000000000000 ) ) ;
#3538=ADVANCED_FACE ( 'NONE', ( #2774 ), #14750, .F. ) ;
#3564=MANIFOLD_SOLID_BREP ( 'Body', #4350 ) ;
#3578=CIRCLE ( 'NONE', #7219, 30.39999999999999858 ) ;
#3633=FACE_BOUND ( 'NONE', #4197, .T. ) ;
#3654=VECTOR ( 'NONE', #18615, 1000.000000000000000 ) ;
#3691=ORIENTED_EDGE ( 'NONE', *, *, #15271, .T. ) ;
#3695=CARTESIAN_POINT ( 'NONE',  ( 2.250000000000000000, -27.60846790388774608, -2.000000000000000000 ) ) ;
#3722=FACE_BOUND ( 'NONE', #14975, .T. ) ;
#3731=ORIENTED_EDGE ( 'NONE', *, *, #644, .F. ) ;
#3776=EDGE_CURVE ( 'NONE', #16740, #16445, #11228, .T. ) ;
#3809=CARTESIAN_POINT ( 'NONE',  ( 5.032868406504333869, -28.36021363089093938, -2.000000000000000000 ) ) ;
#3840=EDGE_LOOP ( 'NONE', ( #10422, #1041, #1900, #11359 ) ) ;
#3874=VECTOR ( 'NONE', #9306, 1000.000000000000000 ) ;
#3876=CARTESIAN_POINT ( 'NONE',  ( 0.4999999999999916733, -30.39588787977742257, 0.000000000000000000 ) ) ;
#3891=CARTESIAN_POINT ( 'NONE',  ( -4.144923636027600722, -29.35885059145708098, -2.000000000000000000 ) ) ;
#3922=CARTESIAN_POINT ( 'NONE',  ( 0.000000000000000000, 0.000000000000000000, -2.000000000000000000 ) ) ;
#3964=DIRECTION ( 'NONE',  ( 1.000000000000000000, 0.000000000000000000, 0.000000000000000000 ) ) ;
#3988=VERTEX_POINT ( 'NONE', #9887 ) ;
#4009=DIRECTION ( 'NONE',  ( 0.000000000000000000, 0.000000000000000000, 1.000000000000000000 ) ) ;
#4074=CARTESIAN_POINT ( 'NONE',  ( -23.50000000000000355, 2.877919977996280715E-15, -2.000000000000000000 ) ) ;
#4075=VERTEX_POINT ( 'NONE', #355 ) ;
#4113=VERTEX_POINT ( 'NONE', #16828 ) ;
#4121=DIRECTION ( 'NONE',  ( 1.000000000000000000, 0.000000000000000000, 0.000000000000000000 ) ) ;
#4145=LINE ( 'NONE', #14241, #3654 ) ;
#4148=CARTESIAN_POINT ( 'NONE',  ( 5.032868406504335645, -28.36021363089093938, -2.000000000000000000 ) ) ;
#4153=AXIS2_PLACEMENT_3D ( 'NONE', #6766, #1342, #8388 ) ;
#4182=CIRCLE ( 'NONE', #13293, 23.50000000000000355 ) ;
#4197=EDGE_LOOP ( 'NONE', ( #15144, #13402 ) ) ;
#4291=CARTESIAN_POINT ( 'NONE',  ( 0.000000000000000000, 0.000000000000000000, 0.000000000000000000 ) ) ;
#4295=LINE ( 'NONE', #16095, #1413 ) ;
#4330=CIRCLE ( 'NONE', #6757, 27.29487558977753991 ) ;
#4350=CLOSED_SHELL ( 'NONE', ( #6995, #13096, #15004, #17357, #3538, #17864, #17391, #16101, #2044, #16524, #18448, #16531, #2465, #15676, #16002, #10627, #1213, #2516, #16783, #16040, #13549, #6537 ) ) ;
#4371=ORIENTED_EDGE ( 'NONE', *, *, #12808, .T. ) ;
#4377=CYLINDRICAL_SURFACE ( 'NONE', #10841, 30.39999999999999858 ) ;
#4405=EDGE_CURVE ( 'NONE', #5391, #4113, #4702, .T. ) ;
#4437=CARTESIAN_POINT ( 'NONE',  ( -2.250000000000000000, -27.60846790388774608, -2.000000000000000000 ) ) ;
#4476=( LENGTH_UNIT ( ) NAMED_UNIT ( * ) SI_UNIT ( .MILLI., .METRE. ) );
#4508=ORIENTED_EDGE ( 'NONE', *, *, #1856, .F. ) ;
#4518=DIRECTION ( 'NONE',  ( 1.000000000000000000, 0.000000000000000000, 0.000000000000000000 ) ) ;
#4558=DIRECTION ( 'NONE',  ( 1.000000000000000000, 0.000000000000000000, 0.000000000000000000 ) ) ;
#4579=EDGE_CURVE ( 'NONE', #4113, #18014, #15100, .T. ) ;
#4641=AXIS2_PLACEMENT_3D ( 'NONE', #5514, #17137, #12846 ) ;
#4661=VERTEX_POINT ( 'NONE', #15655 ) ;
#4667=CARTESIAN_POINT ( 'NONE',  ( 0.000000000000000000, 0.000000000000000000, -2.000000000000000000 ) ) ;
#4693=CARTESIAN_POINT ( 'NONE',  ( -3.500000000000000888, -27.60846790388774608, -2.000000000000000000 ) ) ;
#4702=LINE ( 'NONE', #1851, #15405 ) ;
#4717=LINE ( 'NONE', #16533, #15668 ) ;
#4810=CIRCLE ( 'NONE', #13953, 4.349594641156948605 ) ;
#4860=DIRECTION ( 'NONE',  ( 0.01644736842105263414, -0.9998647328874152862, 0.000000000000000000 ) ) ;
#4923=EDGE_CURVE ( 'NONE', #18269, #16445, #9636, .T. ) ;
#4938=CYLINDRICAL_SURFACE ( 'NONE', #5368, 1.249999999999999778 ) ;
#4950=LINE ( 'NONE', #18283, #9709 ) ;
#4954=LINE ( 'NONE', #10758, #8098 ) ;
#4959=CARTESIAN_POINT ( 'NONE',  ( 4.249769933734876659, -30.10148593525447680, 0.000000000000000000 ) ) ;
#5016=DIRECTION ( 'NONE',  ( 1.000000000000000000, 0.000000000000000000, 0.000000000000000000 ) ) ;
#5022=ORIENTED_EDGE ( 'NONE', *, *, #12782, .T. ) ;
#5053=AXIS2_PLACEMENT_3D ( 'NONE', #10773, #16594, #4121 ) ;
#5080=CARTESIAN_POINT ( 'NONE',  ( 0.000000000000000000, 1.305124410222461284, 0.000000000000000000 ) ) ;
#5116=ORIENTED_EDGE ( 'NONE', *, *, #10964, .F. ) ;
#5120=CARTESIAN_POINT ( 'NONE',  ( 8.060728450267873768, -24.77235419320996357, -2.000000000000000000 ) ) ;
#5128=DIRECTION ( 'NONE',  ( 0.000000000000000000, 0.000000000000000000, 1.000000000000000000 ) ) ;
#5133=AXIS2_PLACEMENT_3D ( 'NONE', #12079, #3421, #9215 ) ;
#5147=ORIENTED_EDGE ( 'NONE', *, *, #8422, .F. ) ;
#5152=VERTEX_POINT ( 'NONE', #1881 ) ;
#5162=CARTESIAN_POINT ( 'NONE',  ( -2.250000000000000000, -27.60846790388774608, 0.000000000000000000 ) ) ;
#5174=EDGE_CURVE ( 'NONE', #9048, #8021, #3578, .T. ) ;
#5179=EDGE_CURVE ( 'NONE', #298, #4661, #843, .T. ) ;
#5203=CARTESIAN_POINT ( 'NONE',  ( -2.250000000000000000, -27.60846790388774608, -2.000000000000000000 ) ) ;
#5217=CYLINDRICAL_SURFACE ( 'NONE', #14992, 23.50000000000000355 ) ;
#5231=CARTESIAN_POINT ( 'NONE',  ( 0.000000000000000000, 0.000000000000000000, 0.000000000000000000 ) ) ;
#5360=VERTEX_POINT ( 'NONE', #656 ) ;
#5368=AXIS2_PLACEMENT_3D ( 'NONE', #12270, #461, #1888 ) ;
#5391=VERTEX_POINT ( 'NONE', #15032 ) ;
#5394=CIRCLE ( 'NONE', #16035, 23.50000000000000355 ) ;
#5416=CARTESIAN_POINT ( 'NONE',  ( -8.060728450267886203, -24.77235419320996002, -2.000000000000000000 ) ) ;
#5419=EDGE_CURVE ( 'NONE', #4075, #13818, #2659, .T. ) ;
#5424=ORIENTED_EDGE ( 'NONE', *, *, #8900, .T. ) ;
#5459=ORIENTED_EDGE ( 'NONE', *, *, #15873, .T. ) ;
#5487=DIRECTION ( 'NONE',  ( -0.000000000000000000, -0.000000000000000000, -1.000000000000000000 ) ) ;
#5497=ORIENTED_EDGE ( 'NONE', *, *, #11461, .F. ) ;
#5514=CARTESIAN_POINT ( 'NONE',  ( -9.345251662538453630, -28.92794965710190525, -2.000000000000000000 ) ) ;
#5549=AXIS2_PLACEMENT_3D ( 'NONE', #3922, #7132, #15534 ) ;
#5552=ORIENTED_EDGE ( 'NONE', *, *, #10587, .F. ) ;
#5561=PRODUCT_DEFINITION_SHAPE ( 'NONE', 'NONE',  #18184 ) ;
#5572=EDGE_CURVE ( 'NONE', #12788, #280, #12747, .T. ) ;
#5642=DIRECTION ( 'NONE',  ( 0.000000000000000000, 0.000000000000000000, 1.000000000000000000 ) ) ;
#5646=FACE_OUTER_BOUND ( 'NONE', #6443, .T. ) ;
#5685=CARTESIAN_POINT ( 'NONE',  ( 0.000000000000000000, 1.305124410222461284, -2.000000000000000000 ) ) ;
#5696=EDGE_CURVE ( 'NONE', #17469, #17641, #8450, .T. ) ;
#5711=VECTOR ( 'NONE', #5642, 1000.000000000000000 ) ;
#5726=ORIENTED_EDGE ( 'NONE', *, *, #11988, .T. ) ;
#5736=EDGE_CURVE ( 'NONE', #17978, #1435, #2919, .T. ) ;
#5748=CARTESIAN_POINT ( 'NONE',  ( -4.144923636027600722, -29.35885059145708098, 0.000000000000000000 ) ) ;
#5800=CARTESIAN_POINT ( 'NONE',  ( 0.3865131578947368918, -23.49682122285426189, 0.000000000000000000 ) ) ;
#5812=ORIENTED_EDGE ( 'NONE', *, *, #7619, .T. ) ;
#5819=EDGE_CURVE ( 'NONE', #6455, #1018, #4717, .T. ) ;
#5931=LINE ( 'NONE', #7024, #2205 ) ;
#6040=CARTESIAN_POINT ( 'NONE',  ( -4.888507282057958037, -29.45674523562211888, 0.000000000000000000 ) ) ;
#6043=VERTEX_POINT ( 'NONE', #14334 ) ;
#6060=ORIENTED_EDGE ( 'NONE', *, *, #10968, .T. ) ;
#6067=VECTOR ( 'NONE', #18256, 1000.000000000000000 ) ;
#6095=EDGE_CURVE ( 'NONE', #13907, #12788, #8165, .T. ) ;
#6106=CARTESIAN_POINT ( 'NONE',  ( 0.000000000000000000, 0.000000000000000000, -2.000000000000000000 ) ) ;
#6138=CARTESIAN_POINT ( 'NONE',  ( -23.50000000000000355, 2.877919977996280715E-15, 0.000000000000000000 ) ) ;
#6174=DIRECTION ( 'NONE',  ( 0.01644736842105263067, -0.9998647328874151752, 0.000000000000000000 ) ) ;
#6205=EDGE_CURVE ( 'NONE', #7462, #8021, #1566, .T. ) ;
#6212=LINE ( 'NONE', #1742, #11503 ) ;
#6226=EDGE_CURVE ( 'NONE', #3988, #6455, #10898, .T. ) ;
#6256=ORIENTED_EDGE ( 'NONE', *, *, #8900, .F. ) ;
#6281=AXIS2_PLACEMENT_3D ( 'NONE', #12875, #18673, #8663 ) ;
#6287=ORIENTED_EDGE ( 'NONE', *, *, #8988, .T. ) ;
#6338=CARTESIAN_POINT ( 'NONE',  ( -8.060728450267886203, -24.77235419320996002, -2.000000000000000000 ) ) ;
#6349=AXIS2_PLACEMENT_3D ( 'NONE', #9504, #10826, #5016 ) ;
#6354=VERTEX_POINT ( 'NONE', #13660 ) ;
#6370=CARTESIAN_POINT ( 'NONE',  ( 0.000000000000000000, 1.305124410222461284, -2.000000000000000000 ) ) ;
#6440=EDGE_CURVE ( 'NONE', #7515, #12362, #6658, .T. ) ;
#6443=EDGE_LOOP ( 'NONE', ( #15003, #15920, #12938, #14545 ) ) ;
#6455=VERTEX_POINT ( 'NONE', #17370 ) ;
#6537=ADVANCED_FACE ( 'NONE', ( #5646 ), #12895, .F. ) ;
#6640=LINE ( 'NONE', #551, #6067 ) ;
#6644=CYLINDRICAL_SURFACE ( 'NONE', #8693, 1.249999999999999778 ) ;
#6657=DIRECTION ( 'NONE',  ( 1.000000000000000000, 0.000000000000000000, 0.000000000000000000 ) ) ;
#6658=CIRCLE ( 'NONE', #12736, 0.7499999999999997780 ) ;
#6677=DIRECTION ( 'NONE',  ( -0.000000000000000000, -0.000000000000000000, -1.000000000000000000 ) ) ;
#6692=ORIENTED_EDGE ( 'NONE', *, *, #15995, .F. ) ;
#6695=CARTESIAN_POINT ( 'NONE',  ( 0.3865131578947368918, -23.49682122285426189, -2.000000000000000000 ) ) ;
#6750=CARTESIAN_POINT ( 'NONE',  ( -0.9999999999999986677, -27.60846790388774608, -2.000000000000000000 ) ) ;
#6757=AXIS2_PLACEMENT_3D ( 'NONE', #14911, #1854, #17234 ) ;
#6766=CARTESIAN_POINT ( 'NONE',  ( 4.144923636027600722, -29.35885059145708098, -2.000000000000000000 ) ) ;
#6789=DIRECTION ( 'NONE',  ( 1.000000000000000000, 0.000000000000000000, -0.000000000000000000 ) ) ;
#6790=CARTESIAN_POINT ( 'NONE',  ( -4.249769933734879324, -30.10148593525447680, 0.000000000000000000 ) ) ;
#6818=SURFACE_STYLE_FILL_AREA ( #17117 ) ;
#6824=CARTESIAN_POINT ( 'NONE',  ( 0.3865131578947368918, -23.49682122285426189, 0.000000000000000000 ) ) ;
#6827=FACE_OUTER_BOUND ( 'NONE', #7260, .T. ) ;
#6920=AXIS2_PLACEMENT_3D ( 'NONE', #15572, #9557, #3964 ) ;
#6959=DIRECTION ( 'NONE',  ( -1.000000000000000000, 0.000000000000000000, 0.000000000000000000 ) ) ;
#6984=DIRECTION ( 'NONE',  ( 1.000000000000000000, 0.000000000000000000, 0.000000000000000000 ) ) ;
#6995=ADVANCED_FACE ( 'NONE', ( #11892 ), #10561, .F. ) ;
#7024=CARTESIAN_POINT ( 'NONE',  ( -4.888507282057958037, -29.45674523562211888, -2.000000000000000000 ) ) ;
#7049=CYLINDRICAL_SURFACE ( 'NONE', #5549, 23.50000000000000355 ) ;
#7086=CARTESIAN_POINT ( 'NONE',  ( 0.000000000000000000, 1.305124410222461284, 0.000000000000000000 ) ) ;
#7132=DIRECTION ( 'NONE',  ( 0.000000000000000000, 0.000000000000000000, 1.000000000000000000 ) ) ;
#7146=ORIENTED_EDGE ( 'NONE', *, *, #11461, .T. ) ;
#7159=ORIENTED_EDGE ( 'NONE', *, *, #11389, .F. ) ;
#7180=CIRCLE ( 'NONE', #4153, 0.7499999999999997780 ) ;
#7183=FACE_OUTER_BOUND ( 'NONE', #9734, .T. ) ;
#7219=AXIS2_PLACEMENT_3D ( 'NONE', #4291, #8928, #4558 ) ;
#7246=ORIENTED_EDGE ( 'NONE', *, *, #17825, .F. ) ;
#7260=EDGE_LOOP ( 'NONE', ( #13047, #7873, #6060, #12947 ) ) ;
#7303=PRODUCT_DEFINITION_CONTEXT ( 'detailed design', #11199, 'design' ) ;
#7336=AXIS2_PLACEMENT_3D ( 'NONE', #7086, #17381, #1201 ) ;
#7386=DIRECTION ( 'NONE',  ( 0.000000000000000000, 0.000000000000000000, 1.000000000000000000 ) ) ;
#7436=ORIENTED_EDGE ( 'NONE', *, *, #16999, .F. ) ;
#7450=DIRECTION ( 'NONE',  ( 0.1305261922200516844, -0.9914448613738103822, 0.000000000000000000 ) ) ;
#7453=DIRECTION ( 'NONE',  ( 1.000000000000000000, 0.000000000000000000, 0.000000000000000000 ) ) ;
#7462=VERTEX_POINT ( 'NONE', #10609 ) ;
#7479=DIRECTION ( 'NONE',  ( 0.000000000000000000, 0.000000000000000000, 1.000000000000000000 ) ) ;
#7509=ORIENTED_EDGE ( 'NONE', *, *, #5696, .F. ) ;
#7515=VERTEX_POINT ( 'NONE', #6040 ) ;
#7516=CARTESIAN_POINT ( 'NONE',  ( -2.250000000000000000, -27.60846790388774608, -2.000000000000000000 ) ) ;
#7558=CARTESIAN_POINT ( 'NONE',  ( 0.000000000000000000, 0.000000000000000000, -2.000000000000000000 ) ) ;
#7599=VECTOR ( 'NONE', #8145, 1000.000000000000000 ) ;
#7609=CARTESIAN_POINT ( 'NONE',  ( 0.3865131578947368918, -23.49682122285426189, -2.000000000000000000 ) ) ;
#7619=EDGE_CURVE ( 'NONE', #12293, #5152, #867, .T. ) ;
#7620=EDGE_LOOP ( 'NONE', ( #10160, #10331, #10928, #8522 ) ) ;
#7641=DIRECTION ( 'NONE',  ( 0.000000000000000000, 0.000000000000000000, 1.000000000000000000 ) ) ;
#7673=( LENGTH_UNIT ( ) NAMED_UNIT ( * ) SI_UNIT ( .MILLI., .METRE. ) );
#7682=ORIENTED_EDGE ( 'NONE', *, *, #5419, .T. ) ;
#7720=ORIENTED_EDGE ( 'NONE', *, *, #10652, .F. ) ;
#7732=CARTESIAN_POINT ( 'NONE',  ( -0.9999999999999986677, -27.60846790388774608, -2.000000000000000000 ) ) ;
#7873=ORIENTED_EDGE ( 'NONE', *, *, #16567, .F. ) ;
#7910=DIRECTION ( 'NONE',  ( 0.000000000000000000, 0.000000000000000000, 1.000000000000000000 ) ) ;
#7939=CIRCLE ( 'NONE', #7336, 27.29487558977753991 ) ;
#8017=AXIS2_PLACEMENT_3D ( 'NONE', #12801, #14324, #9934 ) ;
#8021=VERTEX_POINT ( 'NONE', #4959 ) ;
#8034=COLOUR_RGB ( '',1.000000000000000000, 0.9490196078431372140, 0.9098039215686274384 ) ;
#8052=ORIENTED_EDGE ( 'NONE', *, *, #6440, .T. ) ;
#8097=FACE_OUTER_BOUND ( 'NONE', #10784, .T. ) ;
#8098=VECTOR ( 'NONE', #16576, 999.9999999999998863 ) ;
#8145=DIRECTION ( 'NONE',  ( 0.000000000000000000, 0.000000000000000000, 1.000000000000000000 ) ) ;
#8146=DIRECTION ( 'NONE',  ( 0.000000000000000000, 0.000000000000000000, 1.000000000000000000 ) ) ;
#8153=AXIS2_PLACEMENT_3D ( 'NONE', #10977, #15561, #13836 ) ;
#8160=AXIS2_PLACEMENT_3D ( 'NONE', #6106, #7910, #677 ) ;
#8162=SHAPE_REPRESENTATION_RELATIONSHIP ( 'NONE' , 'NONE' ,  #2386, #10770 ) ;
#8165=CIRCLE ( 'NONE', #15169, 4.349594641156948605 ) ;
#8198=ORIENTED_EDGE ( 'NONE', *, *, #15995, .T. ) ;
#8200=CARTESIAN_POINT ( 'NONE',  ( -0.3865131578947368918, -23.49682122285426189, -2.000000000000000000 ) ) ;
#8271=DIRECTION ( 'NONE',  ( 0.000000000000000000, 0.000000000000000000, 1.000000000000000000 ) ) ;
#8275=VERTEX_POINT ( 'NONE', #14202 ) ;
#8277=DIRECTION ( 'NONE',  ( 0.000000000000000000, 0.000000000000000000, 1.000000000000000000 ) ) ;
#8316=DIRECTION ( 'NONE',  ( 1.000000000000000000, 0.000000000000000000, 0.000000000000000000 ) ) ;
#8322=DIRECTION ( 'NONE',  ( 1.000000000000000000, 0.000000000000000000, 0.000000000000000000 ) ) ;
#8376=EDGE_LOOP ( 'NONE', ( #13659, #2480, #12817, #15187, #14989, #7146, #16522, #12142, #16899, #17695, #1189, #5812, #2636, #8052, #14411, #5022 ) ) ;
#8382=DIRECTION ( 'NONE',  ( 0.000000000000000000, 0.000000000000000000, 1.000000000000000000 ) ) ;
#8388=DIRECTION ( 'NONE',  ( -1.000000000000000000, 0.000000000000000000, 0.000000000000000000 ) ) ;
#8403=DIRECTION ( 'NONE',  ( 0.000000000000000000, 0.000000000000000000, 1.000000000000000000 ) ) ;
#8410=CARTESIAN_POINT ( 'NONE',  ( -2.250000000000000000, -27.60846790388774608, -2.000000000000000000 ) ) ;
#8420=CARTESIAN_POINT ( 'NONE',  ( 23.50000000000000355, 0.000000000000000000, -2.000000000000000000 ) ) ;
#8422=EDGE_CURVE ( 'NONE', #5360, #596, #265, .T. ) ;
#8427=VECTOR ( 'NONE', #15156, 1000.000000000000000 ) ;
#8444=SURFACE_SIDE_STYLE ('',( #6818 ) ) ;
#8450=CIRCLE ( 'NONE', #10866, 1.249999999999999778 ) ;
#8473=CIRCLE ( 'NONE', #252, 27.29487558977753991 ) ;
#8494=AXIS2_PLACEMENT_3D ( 'NONE', #8410, #11644, #2505 ) ;
#8520=CARTESIAN_POINT ( 'NONE',  ( 0.000000000000000000, 0.000000000000000000, 0.000000000000000000 ) ) ;
#8522=ORIENTED_EDGE ( 'NONE', *, *, #5696, .T. ) ;
#8586=DIRECTION ( 'NONE',  ( 0.000000000000000000, 0.000000000000000000, 1.000000000000000000 ) ) ;
#8590=DIRECTION ( 'NONE',  ( 0.01644736842105263414, 0.9998647328874152862, -0.000000000000000000 ) ) ;
#8647=EDGE_CURVE ( 'NONE', #17978, #13907, #9890, .T. ) ;
#8663=DIRECTION ( 'NONE',  ( 1.000000000000000000, 0.000000000000000000, 0.000000000000000000 ) ) ;
#8681=LINE ( 'NONE', #13076, #5711 ) ;
#8693=AXIS2_PLACEMENT_3D ( 'NONE', #3695, #12452, #11007 ) ;
#8726=CARTESIAN_POINT ( 'NONE',  ( 4.888507282057958925, -29.45674523562211888, -2.000000000000000000 ) ) ;
#8734=VECTOR ( 'NONE', #15183, 1000.000000000000000 ) ;
#8739=FACE_OUTER_BOUND ( 'NONE', #12062, .T. ) ;
#8803=ORIENTED_EDGE ( 'NONE', *, *, #12808, .F. ) ;
#8820=VECTOR ( 'NONE', #2717, 1000.000000000000000 ) ;
#8829=ORIENTED_EDGE ( 'NONE', *, *, #5736, .F. ) ;
#8845=DIRECTION ( 'NONE',  ( 1.000000000000000000, 0.000000000000000000, 0.000000000000000000 ) ) ;
#8900=EDGE_CURVE ( 'NONE', #9845, #17362, #6640, .T. ) ;
#8928=DIRECTION ( 'NONE',  ( 0.000000000000000000, 0.000000000000000000, 1.000000000000000000 ) ) ;
#8932=CARTESIAN_POINT ( 'NONE',  ( 5.032868406504335645, -28.36021363089093938, 0.000000000000000000 ) ) ;
#8945=DIRECTION ( 'NONE',  ( 1.000000000000000000, 0.000000000000000000, 0.000000000000000000 ) ) ;
#8956=AXIS2_PLACEMENT_3D ( 'NONE', #3891, #1565, #7453 ) ;
#8988=EDGE_CURVE ( 'NONE', #16740, #6043, #15201, .T. ) ;
#9001=DIRECTION ( 'NONE',  ( 0.000000000000000000, 0.000000000000000000, 1.000000000000000000 ) ) ;
#9048=VERTEX_POINT ( 'NONE', #3876 ) ;
#9058=ORIENTED_EDGE ( 'NONE', *, *, #5179, .T. ) ;
#9074=CARTESIAN_POINT ( 'NONE',  ( 9.345251662538453630, -28.92794965710190525, -2.000000000000000000 ) ) ;
#9095=VECTOR ( 'NONE', #15704, 1000.000000000000114 ) ;
#9187=ORIENTED_EDGE ( 'NONE', *, *, #4405, .F. ) ;
#9215=DIRECTION ( 'NONE',  ( 1.000000000000000000, 0.000000000000000000, 0.000000000000000000 ) ) ;
#9255=CARTESIAN_POINT ( 'NONE',  ( -5.032868406504333869, -28.36021363089093938, -2.000000000000000000 ) ) ;
#9258=FACE_BOUND ( 'NONE', #14884, .T. ) ;
#9268=DIRECTION ( 'NONE',  ( 0.000000000000000000, 0.000000000000000000, 1.000000000000000000 ) ) ;
#9274=EDGE_CURVE ( 'NONE', #6354, #5152, #13955, .T. ) ;
#9278=ORIENTED_EDGE ( 'NONE', *, *, #6095, .T. ) ;
#9306=DIRECTION ( 'NONE',  ( 0.000000000000000000, 0.000000000000000000, 1.000000000000000000 ) ) ;
#9337=VERTEX_POINT ( 'NONE', #2326 ) ;
#9393=ORIENTED_EDGE ( 'NONE', *, *, #11950, .T. ) ;
#9427=DIRECTION ( 'NONE',  ( 0.000000000000000000, 0.000000000000000000, 1.000000000000000000 ) ) ;
#9443=EDGE_CURVE ( 'NONE', #298, #17641, #4145, .T. ) ;
#9504=CARTESIAN_POINT ( 'NONE',  ( 0.000000000000000000, 0.000000000000000000, -2.000000000000000000 ) ) ;
#9557=DIRECTION ( 'NONE',  ( 0.000000000000000000, 0.000000000000000000, 1.000000000000000000 ) ) ;
#9586=ORIENTED_EDGE ( 'NONE', *, *, #4405, .T. ) ;
#9636=CIRCLE ( 'NONE', #16335, 1.250000000000001110 ) ;
#9655=DIRECTION ( 'NONE',  ( 1.000000000000000000, 0.000000000000000000, 0.000000000000000000 ) ) ;
#9664=VECTOR ( 'NONE', #1033, 1000.000000000000000 ) ;
#9684=AXIS2_PLACEMENT_3D ( 'NONE', #9074, #7641, #16700 ) ;
#9709=VECTOR ( 'NONE', #12380, 999.9999999999998863 ) ;
#9718=DIRECTION ( 'NONE',  ( 0.01644736842105263067, 0.9998647328874151752, 0.000000000000000000 ) ) ;
#9734=EDGE_LOOP ( 'NONE', ( #11173, #15029, #17526, #9905 ) ) ;
#9754=DIRECTION ( 'NONE',  ( 0.000000000000000000, 0.000000000000000000, 1.000000000000000000 ) ) ;
#9760=CARTESIAN_POINT ( 'NONE',  ( 5.032868406504335645, -28.36021363089093938, -2.000000000000000000 ) ) ;
#9812=CARTESIAN_POINT ( 'NONE',  ( 3.499999999999999556, -27.60846790388774608, 0.000000000000000000 ) ) ;
#9845=VERTEX_POINT ( 'NONE', #6695 ) ;
#9887=CARTESIAN_POINT ( 'NONE',  ( -4.249769933734879324, -30.10148593525447680, -2.000000000000000000 ) ) ;
#9890=LINE ( 'NONE', #2467, #9095 ) ;
#9905=ORIENTED_EDGE ( 'NONE', *, *, #16567, .T. ) ;
#9921=DIRECTION ( 'NONE',  ( 1.000000000000000000, 0.000000000000000000, 0.000000000000000000 ) ) ;
#9934=DIRECTION ( 'NONE',  ( 1.000000000000000000, 0.000000000000000000, 0.000000000000000000 ) ) ;
#10004=CARTESIAN_POINT ( 'NONE',  ( 2.250000000000000000, -27.60846790388774608, 0.000000000000000000 ) ) ;
#10039=EDGE_CURVE ( 'NONE', #17362, #9048, #17910, .T. ) ;
#10040=ORIENTED_EDGE ( 'NONE', *, *, #5179, .F. ) ;
#10083=VECTOR ( 'NONE', #15284, 1000.000000000000000 ) ;
#10142=DIRECTION ( 'NONE',  ( -0.9914448613738104932, -0.1305261922200517399, 0.000000000000000000 ) ) ;
#10160=ORIENTED_EDGE ( 'NONE', *, *, #9443, .F. ) ;
#10165=VERTEX_POINT ( 'NONE', #4074 ) ;
#10258=AXIS2_PLACEMENT_3D ( 'NONE', #5685, #7386, #13116 ) ;
#10331=ORIENTED_EDGE ( 'NONE', *, *, #15364, .F. ) ;
#10389=EDGE_CURVE ( 'NONE', #6043, #16740, #11297, .T. ) ;
#10422=ORIENTED_EDGE ( 'NONE', *, *, #10389, .F. ) ;
#10451=DIRECTION ( 'NONE',  ( 0.000000000000000000, 0.000000000000000000, 1.000000000000000000 ) ) ;
#10514=EDGE_CURVE ( 'NONE', #906, #8275, #2057, .T. ) ;
#10561=CYLINDRICAL_SURFACE ( 'NONE', #16116, 1.250000000000001110 ) ;
#10587=EDGE_CURVE ( 'NONE', #18014, #12293, #7939, .T. ) ;
#10609=CARTESIAN_POINT ( 'NONE',  ( 4.249769933734876659, -30.10148593525447680, -2.000000000000000000 ) ) ;
#10627=ADVANCED_FACE ( 'NONE', ( #14419 ), #2433, .T. ) ;
#10652=EDGE_CURVE ( 'NONE', #596, #8275, #3095, .T. ) ;
#10653=CYLINDRICAL_SURFACE ( 'NONE', #5133, 27.29487558977753991 ) ;
#10662=EDGE_CURVE ( 'NONE', #13907, #2471, #15665, .T. ) ;
#10685=LINE ( 'NONE', #9255, #11439 ) ;
#10701=CIRCLE ( 'NONE', #18002, 1.249999999999999778 ) ;
#10705=CARTESIAN_POINT ( 'NONE',  ( -5.032868406504333869, -28.36021363089093938, -2.000000000000000000 ) ) ;
#10718=( NAMED_UNIT ( * ) PLANE_ANGLE_UNIT ( ) SI_UNIT ( $, .RADIAN. ) );
#10753=PLANE ( 'NONE',  #17602 ) ;
#10756=LINE ( 'NONE', #10848, #8427 ) ;
#10758=CARTESIAN_POINT ( 'NONE',  ( -0.3865131578947368918, -23.49682122285426189, 0.000000000000000000 ) ) ;
#10770=ADVANCED_BREP_SHAPE_REPRESENTATION ( '', ( #3564, #8017 ), #3170 ) ;
#10773=CARTESIAN_POINT ( 'NONE',  ( -4.144923636027600722, -29.35885059145708098, -2.000000000000000000 ) ) ;
#10784=EDGE_LOOP ( 'NONE', ( #11693, #8829, #10942, #3165 ) ) ;
#10826=DIRECTION ( 'NONE',  ( -0.000000000000000000, -0.000000000000000000, -1.000000000000000000 ) ) ;
#10841=AXIS2_PLACEMENT_3D ( 'NONE', #1156, #4009, #17426 ) ;
#10846=FACE_OUTER_BOUND ( 'NONE', #8376, .T. ) ;
#10848=CARTESIAN_POINT ( 'NONE',  ( -27.29487558977753991, 1.305124410222464393, -2.000000000000000000 ) ) ;
#10865=ORIENTED_EDGE ( 'NONE', *, *, #5174, .F. ) ;
#10866=AXIS2_PLACEMENT_3D ( 'NONE', #2642, #13121, #12928 ) ;
#10898=CIRCLE ( 'NONE', #2702, 30.39999999999999858 ) ;
#10902=AXIS2_PLACEMENT_3D ( 'NONE', #14954, #1894, #14753 ) ;
#10910=CARTESIAN_POINT ( 'NONE',  ( -3.500000000000000888, -27.60846790388774608, 0.000000000000000000 ) ) ;
#10928=ORIENTED_EDGE ( 'NONE', *, *, #1856, .T. ) ;
#10942=ORIENTED_EDGE ( 'NONE', *, *, #8647, .T. ) ;
#10964=EDGE_CURVE ( 'NONE', #6354, #12492, #10685, .T. ) ;
#10968=EDGE_CURVE ( 'NONE', #12492, #3988, #17531, .T. ) ;
#10977=CARTESIAN_POINT ( 'NONE',  ( -9.345251662538453630, -28.92794965710190525, 0.000000000000000000 ) ) ;
#10979=EDGE_LOOP ( 'NONE', ( #18356, #2442, #457, #17026, #5116, #7246, #17167, #12224, #2899, #13354, #11599, #8803, #12927, #6692, #16051, #14948 ) ) ;
#11007=DIRECTION ( 'NONE',  ( 1.000000000000000000, 0.000000000000000000, 0.000000000000000000 ) ) ;
#11025=CIRCLE ( 'NONE', #13764, 23.50000000000000355 ) ;
#11096=SURFACE_STYLE_USAGE ( .BOTH. , #8444 ) ;
#11134=DIRECTION ( 'NONE',  ( 0.9998647328874151752, -0.01644736842105263067, 0.000000000000000000 ) ) ;
#11173=ORIENTED_EDGE ( 'NONE', *, *, #15650, .F. ) ;
#11199=APPLICATION_CONTEXT ( 'automotive_design' ) ;
#11216=DIRECTION ( 'NONE',  ( 0.000000000000000000, 0.000000000000000000, 1.000000000000000000 ) ) ;
#11228=LINE ( 'NONE', #6750, #17208 ) ;
#11244=DIRECTION ( 'NONE',  ( 1.000000000000000000, 0.000000000000000000, 0.000000000000000000 ) ) ;
#11284=DIRECTION ( 'NONE',  ( 1.000000000000000000, 0.000000000000000000, 0.000000000000000000 ) ) ;
#11297=CIRCLE ( 'NONE', #649, 1.250000000000001110 ) ;
#11307=FACE_OUTER_BOUND ( 'NONE', #1950, .T. ) ;
#11315=ORIENTED_EDGE ( 'NONE', *, *, #10514, .F. ) ;
#11327=PRODUCT ( 'circlip for shafts normal_din_Circlip DIN 471 - 50 x 2', 'circlip for shafts normal_din_Circlip DIN 471 - 50 x 2', '', ( #3082 ) ) ;
#11359=ORIENTED_EDGE ( 'NONE', *, *, #3776, .F. ) ;
#11389=EDGE_CURVE ( 'NONE', #4075, #18014, #10756, .T. ) ;
#11439=VECTOR ( 'NONE', #15077, 1000.000000000000114 ) ;
#11461=EDGE_CURVE ( 'NONE', #8021, #1435, #13292, .T. ) ;
#11503=VECTOR ( 'NONE', #7450, 1000.000000000000114 ) ;
#11541=AXIS2_PLACEMENT_3D ( 'NONE', #7609, #367, #6174 ) ;
#11599=ORIENTED_EDGE ( 'NONE', *, *, #8647, .F. ) ;
#11622=DIRECTION ( 'NONE',  ( 1.000000000000000000, 0.000000000000000000, 0.000000000000000000 ) ) ;
#11641=DIRECTION ( 'NONE',  ( 0.000000000000000000, 0.000000000000000000, 1.000000000000000000 ) ) ;
#11644=DIRECTION ( 'NONE',  ( 0.000000000000000000, 0.000000000000000000, 1.000000000000000000 ) ) ;
#11650=SHAPE_DEFINITION_REPRESENTATION ( #5561, #2386 ) ;
#11662=DIRECTION ( 'NONE',  ( -0.000000000000000000, -0.000000000000000000, -1.000000000000000000 ) ) ;
#11684=UNCERTAINTY_MEASURE_WITH_UNIT (LENGTH_MEASURE( 1.000000000000000082E-05 ), #18254, 'distance_accuracy_value', 'NONE');
#11693=ORIENTED_EDGE ( 'NONE', *, *, #13681, .F. ) ;
#11799=EDGE_CURVE ( 'NONE', #14286, #9048, #3508, .T. ) ;
#11821=DIRECTION ( 'NONE',  ( -0.000000000000000000, -0.000000000000000000, -1.000000000000000000 ) ) ;
#11823=AXIS2_PLACEMENT_3D ( 'NONE', #5231, #9427, #12570 ) ;
#11892=FACE_OUTER_BOUND ( 'NONE', #3840, .T. ) ;
#11931=FACE_OUTER_BOUND ( 'NONE', #18280, .T. ) ;
#11936=DIRECTION ( 'NONE',  ( 1.000000000000000000, 0.000000000000000000, 0.000000000000000000 ) ) ;
#11950=EDGE_CURVE ( 'NONE', #10165, #906, #5394, .T. ) ;
#11982=DIRECTION ( 'NONE',  ( 1.000000000000000000, 0.000000000000000000, 0.000000000000000000 ) ) ;
#11988=EDGE_CURVE ( 'NONE', #13818, #12293, #18456, .T. ) ;
#12016=CYLINDRICAL_SURFACE ( 'NONE', #9684, 4.349594641156948605 ) ;
#12019=LINE ( 'NONE', #4693, #8734 ) ;
#12062=EDGE_LOOP ( 'NONE', ( #3691, #9586, #3731, #17093 ) ) ;
#12079=CARTESIAN_POINT ( 'NONE',  ( 0.000000000000000000, 1.305124410222461284, -2.000000000000000000 ) ) ;
#12112=ORIENTED_EDGE ( 'NONE', *, *, #11389, .T. ) ;
#12142=ORIENTED_EDGE ( 'NONE', *, *, #2115, .T. ) ;
#12159=EDGE_LOOP ( 'NONE', ( #7436, #782, #2700, #16391 ) ) ;
#12178=DIRECTION ( 'NONE',  ( 1.000000000000000000, 0.000000000000000000, 0.000000000000000000 ) ) ;
#12224=ORIENTED_EDGE ( 'NONE', *, *, #15873, .F. ) ;
#12270=CARTESIAN_POINT ( 'NONE',  ( 2.250000000000000000, -27.60846790388774608, -2.000000000000000000 ) ) ;
#12276=CARTESIAN_POINT ( 'NONE',  ( 0.9999999999999997780, -27.60846790388774608, -2.000000000000000000 ) ) ;
#12289=EDGE_CURVE ( 'NONE', #6455, #9337, #18792, .T. ) ;
#12293=VERTEX_POINT ( 'NONE', #18691 ) ;
#12307=EDGE_LOOP ( 'NONE', ( #15691, #3373, #688, #15545 ) ) ;
#12337=ORIENTED_EDGE ( 'NONE', *, *, #6205, .T. ) ;
#12362=VERTEX_POINT ( 'NONE', #6790 ) ;
#12380=DIRECTION ( 'NONE',  ( 0.01644736842105263414, -0.9998647328874152862, 0.000000000000000000 ) ) ;
#12385=AXIS2_PLACEMENT_3D ( 'NONE', #13141, #96, #8316 ) ;
#12392=CIRCLE ( 'NONE', #6920, 27.29487558977753991 ) ;
#12408=DIRECTION ( 'NONE',  ( 0.000000000000000000, 0.000000000000000000, 1.000000000000000000 ) ) ;
#12452=DIRECTION ( 'NONE',  ( 0.000000000000000000, 0.000000000000000000, 1.000000000000000000 ) ) ;
#12478=FACE_OUTER_BOUND ( 'NONE', #12307, .T. ) ;
#12492=VERTEX_POINT ( 'NONE', #1823 ) ;
#12523=DIRECTION ( 'NONE',  ( 1.000000000000000000, 0.000000000000000000, 0.000000000000000000 ) ) ;
#12570=DIRECTION ( 'NONE',  ( 1.000000000000000000, 0.000000000000000000, -0.000000000000000000 ) ) ;
#12703=EDGE_LOOP ( 'NONE', ( #10865, #936, #18625, #12337 ) ) ;
#12731=PRESENTATION_STYLE_ASSIGNMENT (( #11096 ) ) ;
#12736=AXIS2_PLACEMENT_3D ( 'NONE', #5748, #14119, #8322 ) ;
#12747=LINE ( 'NONE', #5120, #9664 ) ;
#12782=EDGE_CURVE ( 'NONE', #1018, #5360, #4954, .T. ) ;
#12788=VERTEX_POINT ( 'NONE', #3534 ) ;
#12791=APPLICATION_CONTEXT ( 'automotive_design' ) ;
#12801=CARTESIAN_POINT ( 'NONE',  ( 0.000000000000000000, 0.000000000000000000, 0.000000000000000000 ) ) ;
#12808=EDGE_CURVE ( 'NONE', #7462, #17978, #7180, .T. ) ;
#12817=ORIENTED_EDGE ( 'NONE', *, *, #17629, .T. ) ;
#12846=DIRECTION ( 'NONE',  ( 1.000000000000000000, 0.000000000000000000, 0.000000000000000000 ) ) ;
#12864=DIRECTION ( 'NONE',  ( 1.000000000000000000, 0.000000000000000000, 0.000000000000000000 ) ) ;
#12875=CARTESIAN_POINT ( 'NONE',  ( 0.000000000000000000, 0.000000000000000000, -2.000000000000000000 ) ) ;
#12895=CYLINDRICAL_SURFACE ( 'NONE', #8494, 1.250000000000001110 ) ;
#12909=DIRECTION ( 'NONE',  ( 1.000000000000000000, 0.000000000000000000, 0.000000000000000000 ) ) ;
#12918=MECHANICAL_DESIGN_GEOMETRIC_PRESENTATION_REPRESENTATION('',(#18688),#148);
#12921=EDGE_CURVE ( 'NONE', #10165, #596, #4295, .T. ) ;
#12927=ORIENTED_EDGE ( 'NONE', *, *, #17159, .F. ) ;
#12928=DIRECTION ( 'NONE',  ( 1.000000000000000000, 0.000000000000000000, 0.000000000000000000 ) ) ;
#12938=ORIENTED_EDGE ( 'NONE', *, *, #3776, .T. ) ;
#12947=ORIENTED_EDGE ( 'NONE', *, *, #1620, .T. ) ;
#12962=( NAMED_UNIT ( * ) PLANE_ANGLE_UNIT ( ) SI_UNIT ( $, .RADIAN. ) );
#12975=ORIENTED_EDGE ( 'NONE', *, *, #10389, .T. ) ;
#13008=PLANE ( 'NONE',  #3453 ) ;
#13044=DIRECTION ( 'NONE',  ( 1.000000000000000000, 0.000000000000000000, 0.000000000000000000 ) ) ;
#13047=ORIENTED_EDGE ( 'NONE', *, *, #6440, .F. ) ;
#13060=( NAMED_UNIT ( * ) SI_UNIT ( $, .STERADIAN. ) SOLID_ANGLE_UNIT ( ) );
#13073=CARTESIAN_POINT ( 'NONE',  ( 0.000000000000000000, 1.305124410222461284, -2.000000000000000000 ) ) ;
#13076=CARTESIAN_POINT ( 'NONE',  ( 3.499999999999999556, -27.60846790388774608, -2.000000000000000000 ) ) ;
#13096=ADVANCED_FACE ( 'NONE', ( #14947 ), #4938, .F. ) ;
#13116=DIRECTION ( 'NONE',  ( 1.000000000000000000, 0.000000000000000000, 0.000000000000000000 ) ) ;
#13121=DIRECTION ( 'NONE',  ( 0.000000000000000000, 0.000000000000000000, 1.000000000000000000 ) ) ;
#13141=CARTESIAN_POINT ( 'NONE',  ( 2.250000000000000000, -27.60846790388774608, -2.000000000000000000 ) ) ;
#13263=CARTESIAN_POINT ( 'NONE',  ( -5.032868406504333869, -28.36021363089093938, -2.000000000000000000 ) ) ;
#13275=CARTESIAN_POINT ( 'NONE',  ( -9.345251662538453630, -28.92794965710190525, -2.000000000000000000 ) ) ;
#13292=CIRCLE ( 'NONE', #14497, 0.7499999999999997780 ) ;
#13293=AXIS2_PLACEMENT_3D ( 'NONE', #4667, #11821, #8945 ) ;
#13300=DIRECTION ( 'NONE',  ( 1.000000000000000000, 0.000000000000000000, 0.000000000000000000 ) ) ;
#13319=VECTOR ( 'NONE', #14540, 1000.000000000000000 ) ;
#13335=CARTESIAN_POINT ( 'NONE',  ( 0.000000000000000000, 0.000000000000000000, 0.000000000000000000 ) ) ;
#13354=ORIENTED_EDGE ( 'NONE', *, *, #6095, .F. ) ;
#13402=ORIENTED_EDGE ( 'NONE', *, *, #4923, .F. ) ;
#13491=EDGE_LOOP ( 'NONE', ( #7159, #7682, #5726, #5552 ) ) ;
#13549=ADVANCED_FACE ( 'NONE', ( #741 ), #6644, .F. ) ;
#13659=ORIENTED_EDGE ( 'NONE', *, *, #8422, .T. ) ;
#13660=CARTESIAN_POINT ( 'NONE',  ( -5.032868406504333869, -28.36021363089093938, -2.000000000000000000 ) ) ;
#13667=ORIENTED_EDGE ( 'NONE', *, *, #11799, .T. ) ;
#13681=EDGE_CURVE ( 'NONE', #1435, #2471, #17209, .T. ) ;
#13764=AXIS2_PLACEMENT_3D ( 'NONE', #13335, #3231, #11622 ) ;
#13778=EDGE_LOOP ( 'NONE', ( #11315, #17062, #5424, #16246 ) ) ;
#13818=VERTEX_POINT ( 'NONE', #6338 ) ;
#13825=AXIS2_PLACEMENT_3D ( 'NONE', #13275, #15689, #4518 ) ;
#13836=DIRECTION ( 'NONE',  ( 1.000000000000000000, 0.000000000000000000, 0.000000000000000000 ) ) ;
#13862=( NAMED_UNIT ( * ) SI_UNIT ( $, .STERADIAN. ) SOLID_ANGLE_UNIT ( ) );
#13863=ORIENTED_EDGE ( 'NONE', *, *, #9443, .T. ) ;
#13907=VERTEX_POINT ( 'NONE', #9760 ) ;
#13953=AXIS2_PLACEMENT_3D ( 'NONE', #2193, #6677, #11244 ) ;
#13955=LINE ( 'NONE', #10705, #7599 ) ;
#14050=DIRECTION ( 'NONE',  ( 0.000000000000000000, 0.000000000000000000, 1.000000000000000000 ) ) ;
#14076=DIRECTION ( 'NONE',  ( 1.000000000000000000, 0.000000000000000000, 0.000000000000000000 ) ) ;
#14119=DIRECTION ( 'NONE',  ( 0.000000000000000000, 0.000000000000000000, 1.000000000000000000 ) ) ;
#14137=DIRECTION ( 'NONE',  ( 1.000000000000000000, 0.000000000000000000, 0.000000000000000000 ) ) ;
#14165=CYLINDRICAL_SURFACE ( 'NONE', #13825, 4.349594641156947716 ) ;
#14168=DIRECTION ( 'NONE',  ( 0.000000000000000000, 0.000000000000000000, 1.000000000000000000 ) ) ;
#14194=FACE_OUTER_BOUND ( 'NONE', #12703, .T. ) ;
#14202=CARTESIAN_POINT ( 'NONE',  ( 23.50000000000000355, 0.000000000000000000, 0.000000000000000000 ) ) ;
#14239=VECTOR ( 'NONE', #604, 1000.000000000000000 ) ;
#14241=CARTESIAN_POINT ( 'NONE',  ( 0.9999999999999997780, -27.60846790388774608, -2.000000000000000000 ) ) ;
#14273=CARTESIAN_POINT ( 'NONE',  ( 4.888507282057958925, -29.45674523562211888, 0.000000000000000000 ) ) ;
#14286=VERTEX_POINT ( 'NONE', #16414 ) ;
#14324=DIRECTION ( 'NONE',  ( 0.000000000000000000, 0.000000000000000000, 1.000000000000000000 ) ) ;
#14334=CARTESIAN_POINT ( 'NONE',  ( -3.500000000000000888, -27.60846790388774608, -2.000000000000000000 ) ) ;
#14411=ORIENTED_EDGE ( 'NONE', *, *, #16999, .T. ) ;
#14419=FACE_OUTER_BOUND ( 'NONE', #406, .T. ) ;
#14497=AXIS2_PLACEMENT_3D ( 'NONE', #963, #8382, #6959 ) ;
#14540=DIRECTION ( 'NONE',  ( 0.000000000000000000, 0.000000000000000000, 1.000000000000000000 ) ) ;
#14541=ORIENTED_EDGE ( 'NONE', *, *, #6205, .F. ) ;
#14545=ORIENTED_EDGE ( 'NONE', *, *, #15830, .T. ) ;
#14556=CARTESIAN_POINT ( 'NONE',  ( 0.000000000000000000, 1.305124410222461284, -2.000000000000000000 ) ) ;
#14594=ORIENTED_EDGE ( 'NONE', *, *, #10662, .F. ) ;
#14627=CARTESIAN_POINT ( 'NONE',  ( 5.032868406504333869, -28.36021363089093938, 0.000000000000000000 ) ) ;
#14670=CIRCLE ( 'NONE', #4641, 4.349594641156947716 ) ;
#14678=DIRECTION ( 'NONE',  ( 0.000000000000000000, 0.000000000000000000, 1.000000000000000000 ) ) ;
#14697=EDGE_CURVE ( 'NONE', #906, #9845, #4182, .T. ) ;
#14699=CARTESIAN_POINT ( 'NONE',  ( -0.3865131578947368918, -23.49682122285426189, -2.000000000000000000 ) ) ;
#14750=CYLINDRICAL_SURFACE ( 'NONE', #6281, 23.50000000000000355 ) ;
#14753=DIRECTION ( 'NONE',  ( 1.000000000000000000, 0.000000000000000000, 0.000000000000000000 ) ) ;
#14791=FACE_OUTER_BOUND ( 'NONE', #10979, .T. ) ;
#14884=EDGE_LOOP ( 'NONE', ( #6287, #12975 ) ) ;
#14911=CARTESIAN_POINT ( 'NONE',  ( 0.000000000000000000, 1.305124410222461284, 0.000000000000000000 ) ) ;
#14939=EDGE_LOOP ( 'NONE', ( #17021, #6256, #8198, #13667 ) ) ;
#14947=FACE_OUTER_BOUND ( 'NONE', #18647, .T. ) ;
#14948=ORIENTED_EDGE ( 'NONE', *, *, #11950, .F. ) ;
#14954=CARTESIAN_POINT ( 'NONE',  ( 0.000000000000000000, 0.000000000000000000, 0.000000000000000000 ) ) ;
#14975=EDGE_LOOP ( 'NONE', ( #7509, #2450 ) ) ;
#14989=ORIENTED_EDGE ( 'NONE', *, *, #5174, .T. ) ;
#14992=AXIS2_PLACEMENT_3D ( 'NONE', #18562, #8277, #6657 ) ;
#15003=ORIENTED_EDGE ( 'NONE', *, *, #1490, .F. ) ;
#15004=ADVANCED_FACE ( 'NONE', ( #1581 ), #17318, .T. ) ;
#15025=DIRECTION ( 'NONE',  ( 0.000000000000000000, 0.000000000000000000, 1.000000000000000000 ) ) ;
#15029=ORIENTED_EDGE ( 'NONE', *, *, #9274, .F. ) ;
#15032=CARTESIAN_POINT ( 'NONE',  ( 27.29487558977753991, 1.305124410222461284, -2.000000000000000000 ) ) ;
#15055=FACE_OUTER_BOUND ( 'NONE', #12159, .T. ) ;
#15077=DIRECTION ( 'NONE',  ( 0.1305261922200516844, -0.9914448613738103822, 0.000000000000000000 ) ) ;
#15100=CIRCLE ( 'NONE', #2010, 27.29487558977753991 ) ;
#15130=EDGE_LOOP ( 'NONE', ( #18467, #9058 ) ) ;
#15138=FACE_OUTER_BOUND ( 'NONE', #14939, .T. ) ;
#15144=ORIENTED_EDGE ( 'NONE', *, *, #15830, .F. ) ;
#15155=CARTESIAN_POINT ( 'NONE',  ( -0.5000000000000000000, -30.39588787977742257, 0.000000000000000000 ) ) ;
#15156=DIRECTION ( 'NONE',  ( 0.000000000000000000, 0.000000000000000000, 1.000000000000000000 ) ) ;
#15169=AXIS2_PLACEMENT_3D ( 'NONE', #52, #11662, #12909 ) ;
#15183=DIRECTION ( 'NONE',  ( 0.000000000000000000, 0.000000000000000000, 1.000000000000000000 ) ) ;
#15187=ORIENTED_EDGE ( 'NONE', *, *, #10039, .T. ) ;
#15201=CIRCLE ( 'NONE', #296, 1.250000000000001110 ) ;
#15256=AXIS2_PLACEMENT_3D ( 'NONE', #8520, #5487, #11284 ) ;
#15271=EDGE_CURVE ( 'NONE', #12788, #5391, #12392, .T. ) ;
#15284=DIRECTION ( 'NONE',  ( 0.000000000000000000, 0.000000000000000000, 1.000000000000000000 ) ) ;
#15364=EDGE_CURVE ( 'NONE', #4661, #298, #16987, .T. ) ;
#15373=CARTESIAN_POINT ( 'NONE',  ( 2.250000000000000000, -27.60846790388774608, -2.000000000000000000 ) ) ;
#15405=VECTOR ( 'NONE', #9268, 1000.000000000000000 ) ;
#15486=UNCERTAINTY_MEASURE_WITH_UNIT (LENGTH_MEASURE( 1.000000000000000082E-05 ), #4476, 'distance_accuracy_value', 'NONE');
#15534=DIRECTION ( 'NONE',  ( 1.000000000000000000, 0.000000000000000000, 0.000000000000000000 ) ) ;
#15545=ORIENTED_EDGE ( 'NONE', *, *, #1432, .T. ) ;
#15561=DIRECTION ( 'NONE',  ( -0.000000000000000000, -0.000000000000000000, -1.000000000000000000 ) ) ;
#15568=AXIS2_PLACEMENT_3D ( 'NONE', #18790, #11641, #6984 ) ;
#15572=CARTESIAN_POINT ( 'NONE',  ( 0.000000000000000000, 1.305124410222461284, -2.000000000000000000 ) ) ;
#15581=ORIENTED_EDGE ( 'NONE', *, *, #4579, .F. ) ;
#15584=( NAMED_UNIT ( * ) PLANE_ANGLE_UNIT ( ) SI_UNIT ( $, .RADIAN. ) );
#15650=EDGE_CURVE ( 'NONE', #5152, #7515, #6212, .T. ) ;
#15655=CARTESIAN_POINT ( 'NONE',  ( 3.499999999999999556, -27.60846790388774608, -2.000000000000000000 ) ) ;
#15665=LINE ( 'NONE', #4148, #8820 ) ;
#15668=VECTOR ( 'NONE', #9001, 1000.000000000000000 ) ;
#15676=ADVANCED_FACE ( 'NONE', ( #11931 ), #12016, .F. ) ;
#15689=DIRECTION ( 'NONE',  ( 0.000000000000000000, 0.000000000000000000, 1.000000000000000000 ) ) ;
#15691=ORIENTED_EDGE ( 'NONE', *, *, #12782, .F. ) ;
#15704=DIRECTION ( 'NONE',  ( 0.1305261922200516844, 0.9914448613738103822, -0.000000000000000000 ) ) ;
#15710=( GEOMETRIC_REPRESENTATION_CONTEXT ( 3 ) GLOBAL_UNCERTAINTY_ASSIGNED_CONTEXT ( ( #15486 ) ) GLOBAL_UNIT_ASSIGNED_CONTEXT ( ( #4476, #12962, #13060 ) ) REPRESENTATION_CONTEXT ( 'NONE', 'WORKASPACE' ) );
#15738=AXIS2_PLACEMENT_3D ( 'NONE', #6370, #10451, #12178 ) ;
#15820=DIRECTION ( 'NONE',  ( 0.000000000000000000, 0.000000000000000000, 1.000000000000000000 ) ) ;
#15830=EDGE_CURVE ( 'NONE', #16445, #18269, #572, .T. ) ;
#15873=EDGE_CURVE ( 'NONE', #5391, #4075, #8473, .T. ) ;
#15920=ORIENTED_EDGE ( 'NONE', *, *, #8988, .F. ) ;
#15949=DIRECTION ( 'NONE',  ( 0.1305261922200517399, -0.9914448613738104932, 0.000000000000000000 ) ) ;
#15995=EDGE_CURVE ( 'NONE', #9845, #14286, #4950, .T. ) ;
#16002=ADVANCED_FACE ( 'NONE', ( #8097 ), #10753, .T. ) ;
#16035=AXIS2_PLACEMENT_3D ( 'NONE', #16940, #2458, #14076 ) ;
#16040=ADVANCED_FACE ( 'NONE', ( #3633, #3722, #10846 ), #16672, .T. ) ;
#16051=ORIENTED_EDGE ( 'NONE', *, *, #14697, .F. ) ;
#16066=AXIS2_PLACEMENT_3D ( 'NONE', #15373, #8146, #12523 ) ;
#16095=CARTESIAN_POINT ( 'NONE',  ( -23.50000000000000355, 2.877919977996280715E-15, -2.000000000000000000 ) ) ;
#16101=ADVANCED_FACE ( 'NONE', ( #12478 ), #16860, .T. ) ;
#16116=AXIS2_PLACEMENT_3D ( 'NONE', #7516, #17706, #11982 ) ;
#16172=AXIS2_PLACEMENT_3D ( 'NONE', #1720, #14678, #308 ) ;
#16219=ORIENTED_EDGE ( 'NONE', *, *, #5736, .T. ) ;
#16246=ORIENTED_EDGE ( 'NONE', *, *, #17629, .F. ) ;
#16277=CARTESIAN_POINT ( 'NONE',  ( 4.144923636027600722, -29.35885059145708098, -2.000000000000000000 ) ) ;
#16335=AXIS2_PLACEMENT_3D ( 'NONE', #2948, #17341, #12864 ) ;
#16391=ORIENTED_EDGE ( 'NONE', *, *, #5819, .T. ) ;
#16414=CARTESIAN_POINT ( 'NONE',  ( 0.4999999999999916733, -30.39588787977742257, -2.000000000000000000 ) ) ;
#16445=VERTEX_POINT ( 'NONE', #16841 ) ;
#16454=DIRECTION ( 'NONE',  ( 1.000000000000000000, 0.000000000000000000, 0.000000000000000000 ) ) ;
#16514=AXIS2_PLACEMENT_3D ( 'NONE', #7558, #12408, #6789 ) ;
#16522=ORIENTED_EDGE ( 'NONE', *, *, #13681, .T. ) ;
#16524=ADVANCED_FACE ( 'NONE', ( #6827 ), #17043, .T. ) ;
#16531=ADVANCED_FACE ( 'NONE', ( #11307 ), #14165, .F. ) ;
#16533=CARTESIAN_POINT ( 'NONE',  ( -0.5000000000000000000, -30.39588787977742257, -2.000000000000000000 ) ) ;
#16540=ORIENTED_EDGE ( 'NONE', *, *, #17825, .T. ) ;
#16566=EDGE_LOOP ( 'NONE', ( #5459, #12112, #15581, #9187 ) ) ;
#16567=EDGE_CURVE ( 'NONE', #12492, #7515, #5931, .T. ) ;
#16569=DIRECTION ( 'NONE',  ( 0.1305261922200517399, 0.9914448613738104932, 0.000000000000000000 ) ) ;
#16576=DIRECTION ( 'NONE',  ( 0.01644736842105263414, 0.9998647328874152862, -0.000000000000000000 ) ) ;
#16594=DIRECTION ( 'NONE',  ( 0.000000000000000000, 0.000000000000000000, 1.000000000000000000 ) ) ;
#16672=PLANE ( 'NONE',  #11823 ) ;
#16700=DIRECTION ( 'NONE',  ( 1.000000000000000000, 0.000000000000000000, 0.000000000000000000 ) ) ;
#16740=VERTEX_POINT ( 'NONE', #7732 ) ;
#16783=ADVANCED_FACE ( 'NONE', ( #9258, #3178, #14791 ), #1745, .F. ) ;
#16787=CIRCLE ( 'NONE', #16172, 30.39999999999999858 ) ;
#16828=CARTESIAN_POINT ( 'NONE',  ( 27.29487558977753991, 1.305124410222461284, 0.000000000000000000 ) ) ;
#16841=CARTESIAN_POINT ( 'NONE',  ( -0.9999999999999986677, -27.60846790388774608, 0.000000000000000000 ) ) ;
#16860=PLANE ( 'NONE',  #2402 ) ;
#16894=ORIENTED_EDGE ( 'NONE', *, *, #12921, .T. ) ;
#16899=ORIENTED_EDGE ( 'NONE', *, *, #644, .T. ) ;
#16940=CARTESIAN_POINT ( 'NONE',  ( 0.000000000000000000, 0.000000000000000000, -2.000000000000000000 ) ) ;
#16987=CIRCLE ( 'NONE', #16066, 1.249999999999999778 ) ;
#16999=EDGE_CURVE ( 'NONE', #12362, #1018, #2485, .T. ) ;
#17021=ORIENTED_EDGE ( 'NONE', *, *, #10039, .F. ) ;
#17026=ORIENTED_EDGE ( 'NONE', *, *, #10968, .F. ) ;
#17043=CYLINDRICAL_SURFACE ( 'NONE', #8956, 0.7499999999999997780 ) ;
#17062=ORIENTED_EDGE ( 'NONE', *, *, #14697, .T. ) ;
#17093=ORIENTED_EDGE ( 'NONE', *, *, #5572, .F. ) ;
#17117=FILL_AREA_STYLE ('',( #2728 ) ) ;
#17137=DIRECTION ( 'NONE',  ( -0.000000000000000000, -0.000000000000000000, -1.000000000000000000 ) ) ;
#17159=EDGE_CURVE ( 'NONE', #14286, #7462, #16787, .T. ) ;
#17167=ORIENTED_EDGE ( 'NONE', *, *, #5419, .F. ) ;
#17201=ORIENTED_EDGE ( 'NONE', *, *, #9274, .T. ) ;
#17208=VECTOR ( 'NONE', #5128, 1000.000000000000000 ) ;
#17209=LINE ( 'NONE', #14627, #17210 ) ;
#17210=VECTOR ( 'NONE', #17479, 1000.000000000000114 ) ;
#17234=DIRECTION ( 'NONE',  ( 1.000000000000000000, 0.000000000000000000, 0.000000000000000000 ) ) ;
#17307=AXIS2_PLACEMENT_3D ( 'NONE', #5162, #8586, #9921 ) ;
#17318=CYLINDRICAL_SURFACE ( 'NONE', #10258, 27.29487558977753991 ) ;
#17328=CARTESIAN_POINT ( 'NONE',  ( -27.29487558977753991, 1.305124410222464393, 0.000000000000000000 ) ) ;
#17341=DIRECTION ( 'NONE',  ( 0.000000000000000000, 0.000000000000000000, 1.000000000000000000 ) ) ;
#17357=ADVANCED_FACE ( 'NONE', ( #8739 ), #2847, .T. ) ;
#17362=VERTEX_POINT ( 'NONE', #5800 ) ;
#17370=CARTESIAN_POINT ( 'NONE',  ( -0.5000000000000000000, -30.39588787977742257, -2.000000000000000000 ) ) ;
#17381=DIRECTION ( 'NONE',  ( 0.000000000000000000, 0.000000000000000000, 1.000000000000000000 ) ) ;
#17391=ADVANCED_FACE ( 'NONE', ( #2388 ), #7049, .F. ) ;
#17426=DIRECTION ( 'NONE',  ( 1.000000000000000000, 0.000000000000000000, 0.000000000000000000 ) ) ;
#17469=VERTEX_POINT ( 'NONE', #9812 ) ;
#17479=DIRECTION ( 'NONE',  ( 0.1305261922200516844, 0.9914448613738103822, -0.000000000000000000 ) ) ;
#17509=EDGE_CURVE ( 'NONE', #17641, #17469, #10701, .T. ) ;
#17526=ORIENTED_EDGE ( 'NONE', *, *, #10964, .T. ) ;
#17531=CIRCLE ( 'NONE', #5053, 0.7499999999999997780 ) ;
#17536=ORIENTED_EDGE ( 'NONE', *, *, #5572, .T. ) ;
#17593=CARTESIAN_POINT ( 'NONE',  ( 4.888507282057958925, -29.45674523562211888, -2.000000000000000000 ) ) ;
#17602=AXIS2_PLACEMENT_3D ( 'NONE', #3809, #18191, #16569 ) ;
#17629=EDGE_CURVE ( 'NONE', #8275, #17362, #11025, .T. ) ;
#17641=VERTEX_POINT ( 'NONE', #17703 ) ;
#17670=VECTOR ( 'NONE', #4860, 999.9999999999998863 ) ;
#17695=ORIENTED_EDGE ( 'NONE', *, *, #4579, .T. ) ;
#17703=CARTESIAN_POINT ( 'NONE',  ( 0.9999999999999997780, -27.60846790388774608, 0.000000000000000000 ) ) ;
#17706=DIRECTION ( 'NONE',  ( 0.000000000000000000, 0.000000000000000000, 1.000000000000000000 ) ) ;
#17765=UNCERTAINTY_MEASURE_WITH_UNIT (LENGTH_MEASURE( 1.000000000000000082E-05 ), #7673, 'distance_accuracy_value', 'NONE');
#17813=ORIENTED_EDGE ( 'NONE', *, *, #10514, .T. ) ;
#17825=EDGE_CURVE ( 'NONE', #13818, #6354, #14670, .T. ) ;
#17864=ADVANCED_FACE ( 'NONE', ( #1039 ), #5217, .F. ) ;
#17893=CARTESIAN_POINT ( 'NONE',  ( 0.4999999999999916733, -30.39588787977742257, -2.000000000000000000 ) ) ;
#17910=LINE ( 'NONE', #6824, #17670 ) ;
#17940=DIRECTION ( 'NONE',  ( 0.000000000000000000, 0.000000000000000000, 1.000000000000000000 ) ) ;
#17978=VERTEX_POINT ( 'NONE', #17593 ) ;
#17994=CARTESIAN_POINT ( 'NONE',  ( 8.060728450267873768, -24.77235419320996357, 0.000000000000000000 ) ) ;
#18002=AXIS2_PLACEMENT_3D ( 'NONE', #10004, #15820, #8845 ) ;
#18014=VERTEX_POINT ( 'NONE', #17328 ) ;
#18035=ORIENTED_EDGE ( 'NONE', *, *, #12921, .F. ) ;
#18101=VECTOR ( 'NONE', #8590, 999.9999999999998863 ) ;
#18184=PRODUCT_DEFINITION ( 'UNKNOWN', '', #18408, #7303 ) ;
#18191=DIRECTION ( 'NONE',  ( 0.9914448613738104932, -0.1305261922200517399, 0.000000000000000000 ) ) ;
#18254=( LENGTH_UNIT ( ) NAMED_UNIT ( * ) SI_UNIT ( .MILLI., .METRE. ) );
#18256=DIRECTION ( 'NONE',  ( 0.000000000000000000, 0.000000000000000000, 1.000000000000000000 ) ) ;
#18269=VERTEX_POINT ( 'NONE', #10910 ) ;
#18273=EDGE_LOOP ( 'NONE', ( #492, #16894, #5147, #1229 ) ) ;
#18280=EDGE_LOOP ( 'NONE', ( #2266, #14594, #9278, #17536 ) ) ;
#18283=CARTESIAN_POINT ( 'NONE',  ( 0.3865131578947368918, -23.49682122285426189, -2.000000000000000000 ) ) ;
#18356=ORIENTED_EDGE ( 'NONE', *, *, #2597, .F. ) ;
#18408=PRODUCT_DEFINITION_FORMATION_WITH_SPECIFIED_SOURCE ( 'ANY', '', #11327, .NOT_KNOWN. ) ;
#18448=ADVANCED_FACE ( 'NONE', ( #7183 ), #13008, .T. ) ;
#18456=LINE ( 'NONE', #5416, #18717 ) ;
#18467=ORIENTED_EDGE ( 'NONE', *, *, #15364, .T. ) ;
#18562=CARTESIAN_POINT ( 'NONE',  ( 0.000000000000000000, 0.000000000000000000, -2.000000000000000000 ) ) ;
#18608=AXIS2_PLACEMENT_3D ( 'NONE', #16277, #14050, #14137 ) ;
#18615=DIRECTION ( 'NONE',  ( 0.000000000000000000, 0.000000000000000000, 1.000000000000000000 ) ) ;
#18625=ORIENTED_EDGE ( 'NONE', *, *, #17159, .T. ) ;
#18647=EDGE_LOOP ( 'NONE', ( #10040, #13863, #2870, #4508 ) ) ;
#18673=DIRECTION ( 'NONE',  ( 0.000000000000000000, 0.000000000000000000, 1.000000000000000000 ) ) ;
#18688=STYLED_ITEM ( 'NONE', ( #12731 ), #10770 ) ;
#18691=CARTESIAN_POINT ( 'NONE',  ( -8.060728450267886203, -24.77235419320996002, 0.000000000000000000 ) ) ;
#18717=VECTOR ( 'NONE', #14168, 1000.000000000000000 ) ;
#18790=CARTESIAN_POINT ( 'NONE',  ( 0.000000000000000000, 0.000000000000000000, 0.000000000000000000 ) ) ;
#18792=LINE ( 'NONE', #2697, #18101 ) ;
#18870=COLOUR_RGB('Grey',0.48,0.52,0.57);
#18871=FILL_AREA_STYLE_COLOUR('',#18870);
#18872=FILL_AREA_STYLE('',(#18871));
#18873=SURFACE_STYLE_FILL_AREA(#18872);
#18874=SURFACE_SIDE_STYLE('',(#18873));
#18875=SURFACE_STYLE_USAGE(.BOTH.,#18874);
#18876=PRESENTATION_STYLE_ASSIGNMENT((#18875));
ENDSEC;
END-ISO-10303-21;
